ISO-10303-21;
HEADER;
FILE_DESCRIPTION((''),'2;1');
FILE_NAME('Washer_3.step','2026-10-09T10:15:02-07:00',(''),(''),'','','');
FILE_SCHEMA (('AUTOMOTIVE_DESIGN { 1 0 10303 214 3 1 1 }'));
ENDSEC;
DATA;
#10=MECHANICAL_DESIGN_GEOMETRIC_PRESENTATION_REPRESENTATION('',(#87),#6779);
#67=SHAPE_REPRESENTATION_RELATIONSHIP('SRR','None',#6821,#77) ;
#77=ADVANCED_BREP_SHAPE_REPRESENTATION('',(#97),#6773) ;
#87=STYLED_ITEM('',(#6877),#97) ;
#97=MANIFOLD_SOLID_BREP('Body1',#3899) ;
#123=FACE_BOUND('',#770,.T.) ;
#124=FACE_BOUND('',#772,.T.) ;
#219=PLANE('',#4316) ;
#220=PLANE('',#4317) ;
#503=FACE_OUTER_BOUND('',#767,.T.) ;
#504=FACE_OUTER_BOUND('',#768,.T.) ;
#505=FACE_OUTER_BOUND('',#769,.T.) ;
#506=FACE_OUTER_BOUND('',#771,.T.) ;
#767=EDGE_LOOP('',(#3339,#3340,#3341,#3342)) ;
#768=EDGE_LOOP('',(#3343,#3344,#3345,#3346)) ;
#769=EDGE_LOOP('',(#3347)) ;
#770=EDGE_LOOP('',(#3348)) ;
#771=EDGE_LOOP('',(#3349)) ;
#772=EDGE_LOOP('',(#3350)) ;
#1119=LINE('',#6461,#1479) ;
#1120=LINE('',#6467,#1480) ;
#1479=VECTOR('',#5301,6.) ;
#1480=VECTOR('',#5308,3.2) ;
#1679=CIRCLE('',#4311,6.) ;
#1680=CIRCLE('',#4312,6.) ;
#1681=CIRCLE('',#4314,3.2) ;
#1682=CIRCLE('',#4315,3.2) ;
#1947=VERTEX_POINT('',#6458) ;
#1948=VERTEX_POINT('',#6460) ;
#1949=VERTEX_POINT('',#6464) ;
#1950=VERTEX_POINT('',#6466) ;
#2423=EDGE_CURVE('',#1947,#1947,#1679,.T.) ;
#2424=EDGE_CURVE('',#1947,#1948,#1119,.T.) ;
#2425=EDGE_CURVE('',#1948,#1948,#1680,.T.) ;
#2426=EDGE_CURVE('',#1949,#1949,#1681,.T.) ;
#2427=EDGE_CURVE('',#1949,#1950,#1120,.T.) ;
#2428=EDGE_CURVE('',#1950,#1950,#1682,.T.) ;
#3339=ORIENTED_EDGE('',*,*,#2423,.F.) ;
#3340=ORIENTED_EDGE('',*,*,#2424,.T.) ;
#3341=ORIENTED_EDGE('',*,*,#2425,.T.) ;
#3342=ORIENTED_EDGE('',*,*,#2424,.F.) ;
#3343=ORIENTED_EDGE('',*,*,#2426,.F.) ;
#3344=ORIENTED_EDGE('',*,*,#2427,.T.) ;
#3345=ORIENTED_EDGE('',*,*,#2428,.T.) ;
#3346=ORIENTED_EDGE('',*,*,#2427,.F.) ;
#3347=ORIENTED_EDGE('',*,*,#2425,.F.) ;
#3348=ORIENTED_EDGE('',*,*,#2426,.T.) ;
#3349=ORIENTED_EDGE('',*,*,#2423,.T.) ;
#3350=ORIENTED_EDGE('',*,*,#2428,.F.) ;
#3639=CYLINDRICAL_SURFACE('',#4310,6.) ;
#3640=CYLINDRICAL_SURFACE('',#4313,3.2) ;
#3827=ADVANCED_FACE('',(#503),#3639,.T.) ;
#3828=ADVANCED_FACE('',(#504),#3640,.F.) ;
#3829=ADVANCED_FACE('',(#505,#123),#219,.F.) ;
#3830=ADVANCED_FACE('',(#506,#124),#220,.T.) ;
#3899=CLOSED_SHELL('',(#3827,#3828,#3829,#3830)) ;
#4309=AXIS2_PLACEMENT_3D('',#6456,#5295,#5296) ;
#4310=AXIS2_PLACEMENT_3D('',#6457,#5297,#5298) ;
#4311=AXIS2_PLACEMENT_3D('',#6459,#5299,#5300) ;
#4312=AXIS2_PLACEMENT_3D('',#6462,#5302,#5303) ;
#4313=AXIS2_PLACEMENT_3D('',#6463,#5304,#5305) ;
#4314=AXIS2_PLACEMENT_3D('',#6465,#5306,#5307) ;
#4315=AXIS2_PLACEMENT_3D('',#6468,#5309,#5310) ;
#4316=AXIS2_PLACEMENT_3D('',#6469,#5311,#5312) ;
#4317=AXIS2_PLACEMENT_3D('',#6470,#5313,#5314) ;
#5295=DIRECTION('axis',(0.,0.,1.)) ;
#5296=DIRECTION('refdir',(1.,0.,0.)) ;
#5297=DIRECTION('center_axis',(0.,-1.,0.)) ;
#5298=DIRECTION('ref_axis',(1.,0.,0.)) ;
#5299=DIRECTION('center_axis',(0.,-1.,0.)) ;
#5300=DIRECTION('ref_axis',(0.,0.,1.)) ;
#5301=DIRECTION('',(0.,1.,0.)) ;
#5302=DIRECTION('center_axis',(0.,-1.,0.)) ;
#5303=DIRECTION('ref_axis',(0.,0.,1.)) ;
#5304=DIRECTION('center_axis',(0.,-1.,0.)) ;
#5305=DIRECTION('ref_axis',(1.,0.,0.)) ;
#5306=DIRECTION('center_axis',(0.,-1.,0.)) ;
#5307=DIRECTION('ref_axis',(0.,0.,1.)) ;
#5308=DIRECTION('',(0.,-1.,0.)) ;
#5309=DIRECTION('center_axis',(0.,-1.,0.)) ;
#5310=DIRECTION('ref_axis',(0.,0.,1.)) ;
#5311=DIRECTION('center_axis',(0.,-1.,0.)) ;
#5312=DIRECTION('ref_axis',(1.,0.,0.)) ;
#5313=DIRECTION('center_axis',(0.,-1.,0.)) ;
#5314=DIRECTION('ref_axis',(1.,0.,0.)) ;
#6456=CARTESIAN_POINT('',(0.,0.,0.)) ;
#6457=CARTESIAN_POINT('Origin',(35.,-19.5,10.)) ;
#6458=CARTESIAN_POINT('',(29.,-20.,10.)) ;
#6459=CARTESIAN_POINT('Origin',(35.,-20.,10.)) ;
#6460=CARTESIAN_POINT('',(29.,-19.,10.)) ;
#6461=CARTESIAN_POINT('',(29.,-19.5,10.)) ;
#6462=CARTESIAN_POINT('Origin',(35.,-19.,10.)) ;
#6463=CARTESIAN_POINT('Origin',(35.,-19.5,10.)) ;
#6464=CARTESIAN_POINT('',(31.8,-19.,10.)) ;
#6465=CARTESIAN_POINT('Origin',(35.,-19.,10.)) ;
#6466=CARTESIAN_POINT('',(31.8,-20.,10.)) ;
#6467=CARTESIAN_POINT('',(31.8,-19.5,10.)) ;
#6468=CARTESIAN_POINT('Origin',(35.,-20.,10.)) ;
#6469=CARTESIAN_POINT('Origin',(0.,-19.,0.)) ;
#6470=CARTESIAN_POINT('Origin',(0.,-20.,0.)) ;
#6761=UNCERTAINTY_MEASURE_WITH_UNIT(LENGTH_MEASURE(0.01),#6780,
'DISTANCE_ACCURACY_VALUE',
'Maximum model space distance between geometric entities at asserted c
onnectivities') ;
#6767=UNCERTAINTY_MEASURE_WITH_UNIT(LENGTH_MEASURE(0.01),#6780,
'DISTANCE_ACCURACY_VALUE',
'Maximum model space distance between geometric entities at asserted c
onnectivities') ;
#6773=(
GEOMETRIC_REPRESENTATION_CONTEXT(3)
GLOBAL_UNCERTAINTY_ASSIGNED_CONTEXT((#6761))
GLOBAL_UNIT_ASSIGNED_CONTEXT((#6780,#6782,#6783))
REPRESENTATION_CONTEXT('','3D')
) ;
#6779=(
GEOMETRIC_REPRESENTATION_CONTEXT(3)
GLOBAL_UNCERTAINTY_ASSIGNED_CONTEXT((#6767))
GLOBAL_UNIT_ASSIGNED_CONTEXT((#6780,#6782,#6783))
REPRESENTATION_CONTEXT('','3D')
) ;
#6780=(
LENGTH_UNIT()
NAMED_UNIT(*)
SI_UNIT(.MILLI.,.METRE.)
) ;
#6782=(
NAMED_UNIT(*)
PLANE_ANGLE_UNIT()
SI_UNIT($,.RADIAN.)
) ;
#6783=(
NAMED_UNIT(*)
SI_UNIT($,.STERADIAN.)
SOLID_ANGLE_UNIT()
) ;
#6789=SHAPE_DEFINITION_REPRESENTATION(#6800,#6821) ;
#6800=PRODUCT_DEFINITION_SHAPE('',$,#6833) ;
#6821=SHAPE_REPRESENTATION('',(#4309),#6773) ;
#6827=PRODUCT_DEFINITION_CONTEXT('part definition',#6862,'design') ;
#6833=PRODUCT_DEFINITION('Washer_3','Washer_3',#6844,#6827) ;
#6844=PRODUCT_DEFINITION_FORMATION('',$,#6869) ;
#6862=APPLICATION_CONTEXT(
'Core Data for Automotive Mechanical Design Process') ;
#6863=PRODUCT_CONTEXT('part definition',#6862,'mechanical') ;
#6869=PRODUCT('Washer_3','Washer_3',$,(#6863)) ;
#6877=PRESENTATION_STYLE_ASSIGNMENT((#6880)) ;
#6880=SURFACE_STYLE_USAGE(.BOTH.,#6883) ;
#6883=SURFACE_SIDE_STYLE('',(#6886)) ;
#6886=SURFACE_STYLE_FILL_AREA(#6889) ;
#6889=FILL_AREA_STYLE('Opaque(203,203,203)',(#6892)) ;
#6892=FILL_AREA_STYLE_COLOUR('Opaque(203,203,203)',#6895) ;
#6895=COLOUR_RGB('Opaque(203,203,203)', 0.31764706, 0.68627451, 0.89019608) ;
ENDSEC;
END-ISO-10303-21;
